ISO-10303-21;
HEADER;
/* Generated by software containing ST-Developer
 * from STEP Tools, Inc. (www.steptools.com) 
 */

FILE_DESCRIPTION(
/* description */ ('XY cross-slide table'),
/* implementation_level */ '2;1');

FILE_NAME(
/* name */ 'X Stage - 07 Nut bracket.step',
/* time_stamp */ '2026-10-28T03:22:46-07:00',
/* author */ (''),
/* organization */ (''),
/* preprocessor_version */ 'ST-DEVELOPER v20.2',
/* originating_system */ 'Autodesk Translation Framework v15.17.0.0',
/* authorisation */ '');

FILE_SCHEMA (('AUTOMOTIVE_DESIGN { 1 0 10303 214 3 1 1 }'));
ENDSEC;

DATA;
#10=MECHANICAL_DESIGN_GEOMETRIC_PRESENTATION_REPRESENTATION('',(#1708),#62984);
#1527=SHAPE_REPRESENTATION_RELATIONSHIP('SRR','None',#63378,#1610);
#1610=ADVANCED_BREP_SHAPE_REPRESENTATION('',(#1821),#62915);
#1708=STYLED_ITEM('',(#63919),#1821);
#1821=MANIFOLD_SOLID_BREP('Body1',#23002);
#2033=FACE_BOUND('',#4620,.T.);
#2034=FACE_BOUND('',#4621,.T.);
#2035=FACE_BOUND('',#4622,.T.);
#2036=FACE_BOUND('',#4623,.T.);
#2037=FACE_BOUND('',#4626,.T.);
#2038=FACE_BOUND('',#4628,.T.);
#2039=FACE_BOUND('',#4629,.T.);
#2040=FACE_BOUND('',#4630,.T.);
#2041=FACE_BOUND('',#4631,.T.);
#2426=PLANE('',#24614);
#2427=PLANE('',#24618);
#2428=PLANE('',#24622);
#2429=PLANE('',#24626);
#2430=PLANE('',#24630);
#2431=PLANE('',#24634);
#2432=PLANE('',#24638);
#2433=PLANE('',#24642);
#2434=PLANE('',#24643);
#2435=PLANE('',#24644);
#2436=PLANE('',#24645);
#2437=PLANE('',#24646);
#2438=PLANE('',#24647);
#3143=FACE_OUTER_BOUND('',#4603,.T.);
#3144=FACE_OUTER_BOUND('',#4604,.T.);
#3145=FACE_OUTER_BOUND('',#4605,.T.);
#3146=FACE_OUTER_BOUND('',#4606,.T.);
#3147=FACE_OUTER_BOUND('',#4607,.T.);
#3148=FACE_OUTER_BOUND('',#4608,.T.);
#3149=FACE_OUTER_BOUND('',#4609,.T.);
#3150=FACE_OUTER_BOUND('',#4610,.T.);
#3151=FACE_OUTER_BOUND('',#4611,.T.);
#3152=FACE_OUTER_BOUND('',#4612,.T.);
#3153=FACE_OUTER_BOUND('',#4613,.T.);
#3154=FACE_OUTER_BOUND('',#4614,.T.);
#3155=FACE_OUTER_BOUND('',#4615,.T.);
#3156=FACE_OUTER_BOUND('',#4616,.T.);
#3157=FACE_OUTER_BOUND('',#4617,.T.);
#3158=FACE_OUTER_BOUND('',#4618,.T.);
#3159=FACE_OUTER_BOUND('',#4619,.T.);
#3160=FACE_OUTER_BOUND('',#4624,.T.);
#3161=FACE_OUTER_BOUND('',#4625,.T.);
#3162=FACE_OUTER_BOUND('',#4627,.T.);
#3163=FACE_OUTER_BOUND('',#4632,.T.);
#4603=EDGE_LOOP('',(#16108,#16109,#16110,#16111));
#4604=EDGE_LOOP('',(#16112));
#4605=EDGE_LOOP('',(#16113,#16114,#16115,#16116));
#4606=EDGE_LOOP('',(#16117));
#4607=EDGE_LOOP('',(#16118,#16119,#16120,#16121));
#4608=EDGE_LOOP('',(#16122));
#4609=EDGE_LOOP('',(#16123,#16124,#16125,#16126));
#4610=EDGE_LOOP('',(#16127));
#4611=EDGE_LOOP('',(#16128,#16129,#16130,#16131));
#4612=EDGE_LOOP('',(#16132));
#4613=EDGE_LOOP('',(#16133,#16134,#16135,#16136));
#4614=EDGE_LOOP('',(#16137));
#4615=EDGE_LOOP('',(#16138,#16139,#16140,#16141));
#4616=EDGE_LOOP('',(#16142));
#4617=EDGE_LOOP('',(#16143,#16144,#16145,#16146));
#4618=EDGE_LOOP('',(#16147,#16148,#16149,#16150));
#4619=EDGE_LOOP('',(#16151,#16152,#16153,#16154));
#4620=EDGE_LOOP('',(#16155));
#4621=EDGE_LOOP('',(#16156));
#4622=EDGE_LOOP('',(#16157));
#4623=EDGE_LOOP('',(#16158));
#4624=EDGE_LOOP('',(#16159,#16160,#16161,#16162));
#4625=EDGE_LOOP('',(#16163,#16164,#16165,#16166));
#4626=EDGE_LOOP('',(#16167));
#4627=EDGE_LOOP('',(#16168,#16169,#16170,#16171));
#4628=EDGE_LOOP('',(#16172));
#4629=EDGE_LOOP('',(#16173));
#4630=EDGE_LOOP('',(#16174));
#4631=EDGE_LOOP('',(#16175));
#4632=EDGE_LOOP('',(#16176,#16177,#16178,#16179));
#6179=LINE('',#34838,#7666);
#6180=LINE('',#34845,#7667);
#6181=LINE('',#34852,#7668);
#6182=LINE('',#34859,#7669);
#6183=LINE('',#34866,#7670);
#6184=LINE('',#34873,#7671);
#6185=LINE('',#34880,#7672);
#6186=LINE('',#34887,#7673);
#6187=LINE('',#34892,#7674);
#6188=LINE('',#34894,#7675);
#6189=LINE('',#34896,#7676);
#6190=LINE('',#34897,#7677);
#6191=LINE('',#34900,#7678);
#6192=LINE('',#34902,#7679);
#6193=LINE('',#34903,#7680);
#6194=LINE('',#34906,#7681);
#6195=LINE('',#34908,#7682);
#6196=LINE('',#34909,#7683);
#6197=LINE('',#34911,#7684);
#6198=LINE('',#34912,#7685);
#7666=VECTOR('',#27960,0.210000000000001);
#7667=VECTOR('',#27969,0.210000000000001);
#7668=VECTOR('',#27978,0.210000000000001);
#7669=VECTOR('',#27987,0.210000000000001);
#7670=VECTOR('',#27996,0.165);
#7671=VECTOR('',#28005,0.165);
#7672=VECTOR('',#28014,0.165);
#7673=VECTOR('',#28023,1.11);
#7674=VECTOR('',#28028,1.);
#7675=VECTOR('',#28029,1.);
#7676=VECTOR('',#28030,1.);
#7677=VECTOR('',#28031,1.);
#7678=VECTOR('',#28034,1.);
#7679=VECTOR('',#28035,1.);
#7680=VECTOR('',#28036,1.);
#7681=VECTOR('',#28039,1.);
#7682=VECTOR('',#28040,1.);
#7683=VECTOR('',#28041,1.);
#7684=VECTOR('',#28044,1.);
#7685=VECTOR('',#28045,1.);
#9177=CIRCLE('',#24612,0.210000000000001);
#9178=CIRCLE('',#24613,0.210000000000001);
#9179=CIRCLE('',#24616,0.210000000000001);
#9180=CIRCLE('',#24617,0.210000000000001);
#9181=CIRCLE('',#24620,0.210000000000001);
#9182=CIRCLE('',#24621,0.210000000000001);
#9183=CIRCLE('',#24624,0.210000000000001);
#9184=CIRCLE('',#24625,0.210000000000001);
#9185=CIRCLE('',#24628,0.165);
#9186=CIRCLE('',#24629,0.165);
#9187=CIRCLE('',#24632,0.165);
#9188=CIRCLE('',#24633,0.165);
#9189=CIRCLE('',#24636,0.165);
#9190=CIRCLE('',#24637,0.165);
#9191=CIRCLE('',#24640,1.11);
#9192=CIRCLE('',#24641,1.11);
#10189=VERTEX_POINT('',#34835);
#10190=VERTEX_POINT('',#34837);
#10191=VERTEX_POINT('',#34842);
#10192=VERTEX_POINT('',#34844);
#10193=VERTEX_POINT('',#34849);
#10194=VERTEX_POINT('',#34851);
#10195=VERTEX_POINT('',#34856);
#10196=VERTEX_POINT('',#34858);
#10197=VERTEX_POINT('',#34863);
#10198=VERTEX_POINT('',#34865);
#10199=VERTEX_POINT('',#34870);
#10200=VERTEX_POINT('',#34872);
#10201=VERTEX_POINT('',#34877);
#10202=VERTEX_POINT('',#34879);
#10203=VERTEX_POINT('',#34884);
#10204=VERTEX_POINT('',#34886);
#10205=VERTEX_POINT('',#34890);
#10206=VERTEX_POINT('',#34891);
#10207=VERTEX_POINT('',#34893);
#10208=VERTEX_POINT('',#34895);
#10209=VERTEX_POINT('',#34899);
#10210=VERTEX_POINT('',#34901);
#10211=VERTEX_POINT('',#34905);
#10212=VERTEX_POINT('',#34907);
#12438=EDGE_CURVE('',#10189,#10189,#9177,.T.);
#12439=EDGE_CURVE('',#10189,#10190,#6179,.T.);
#12440=EDGE_CURVE('',#10190,#10190,#9178,.T.);
#12441=EDGE_CURVE('',#10191,#10191,#9179,.T.);
#12442=EDGE_CURVE('',#10191,#10192,#6180,.T.);
#12443=EDGE_CURVE('',#10192,#10192,#9180,.T.);
#12444=EDGE_CURVE('',#10193,#10193,#9181,.T.);
#12445=EDGE_CURVE('',#10193,#10194,#6181,.T.);
#12446=EDGE_CURVE('',#10194,#10194,#9182,.T.);
#12447=EDGE_CURVE('',#10195,#10195,#9183,.T.);
#12448=EDGE_CURVE('',#10195,#10196,#6182,.T.);
#12449=EDGE_CURVE('',#10196,#10196,#9184,.T.);
#12450=EDGE_CURVE('',#10197,#10197,#9185,.T.);
#12451=EDGE_CURVE('',#10197,#10198,#6183,.T.);
#12452=EDGE_CURVE('',#10198,#10198,#9186,.T.);
#12453=EDGE_CURVE('',#10199,#10199,#9187,.T.);
#12454=EDGE_CURVE('',#10199,#10200,#6184,.T.);
#12455=EDGE_CURVE('',#10200,#10200,#9188,.T.);
#12456=EDGE_CURVE('',#10201,#10201,#9189,.T.);
#12457=EDGE_CURVE('',#10201,#10202,#6185,.T.);
#12458=EDGE_CURVE('',#10202,#10202,#9190,.T.);
#12459=EDGE_CURVE('',#10203,#10203,#9191,.T.);
#12460=EDGE_CURVE('',#10203,#10204,#6186,.T.);
#12461=EDGE_CURVE('',#10204,#10204,#9192,.T.);
#12462=EDGE_CURVE('',#10205,#10206,#6187,.T.);
#12463=EDGE_CURVE('',#10206,#10207,#6188,.T.);
#12464=EDGE_CURVE('',#10208,#10207,#6189,.T.);
#12465=EDGE_CURVE('',#10205,#10208,#6190,.T.);
#12466=EDGE_CURVE('',#10209,#10205,#6191,.T.);
#12467=EDGE_CURVE('',#10210,#10208,#6192,.T.);
#12468=EDGE_CURVE('',#10209,#10210,#6193,.T.);
#12469=EDGE_CURVE('',#10211,#10209,#6194,.T.);
#12470=EDGE_CURVE('',#10212,#10210,#6195,.T.);
#12471=EDGE_CURVE('',#10211,#10212,#6196,.T.);
#12472=EDGE_CURVE('',#10206,#10211,#6197,.T.);
#12473=EDGE_CURVE('',#10207,#10212,#6198,.T.);
#16108=ORIENTED_EDGE('',*,*,#12438,.F.);
#16109=ORIENTED_EDGE('',*,*,#12439,.T.);
#16110=ORIENTED_EDGE('',*,*,#12440,.F.);
#16111=ORIENTED_EDGE('',*,*,#12439,.F.);
#16112=ORIENTED_EDGE('',*,*,#12438,.T.);
#16113=ORIENTED_EDGE('',*,*,#12441,.F.);
#16114=ORIENTED_EDGE('',*,*,#12442,.T.);
#16115=ORIENTED_EDGE('',*,*,#12443,.F.);
#16116=ORIENTED_EDGE('',*,*,#12442,.F.);
#16117=ORIENTED_EDGE('',*,*,#12441,.T.);
#16118=ORIENTED_EDGE('',*,*,#12444,.F.);
#16119=ORIENTED_EDGE('',*,*,#12445,.T.);
#16120=ORIENTED_EDGE('',*,*,#12446,.F.);
#16121=ORIENTED_EDGE('',*,*,#12445,.F.);
#16122=ORIENTED_EDGE('',*,*,#12444,.T.);
#16123=ORIENTED_EDGE('',*,*,#12447,.F.);
#16124=ORIENTED_EDGE('',*,*,#12448,.T.);
#16125=ORIENTED_EDGE('',*,*,#12449,.F.);
#16126=ORIENTED_EDGE('',*,*,#12448,.F.);
#16127=ORIENTED_EDGE('',*,*,#12447,.T.);
#16128=ORIENTED_EDGE('',*,*,#12450,.F.);
#16129=ORIENTED_EDGE('',*,*,#12451,.T.);
#16130=ORIENTED_EDGE('',*,*,#12452,.F.);
#16131=ORIENTED_EDGE('',*,*,#12451,.F.);
#16132=ORIENTED_EDGE('',*,*,#12450,.T.);
#16133=ORIENTED_EDGE('',*,*,#12453,.F.);
#16134=ORIENTED_EDGE('',*,*,#12454,.T.);
#16135=ORIENTED_EDGE('',*,*,#12455,.F.);
#16136=ORIENTED_EDGE('',*,*,#12454,.F.);
#16137=ORIENTED_EDGE('',*,*,#12453,.T.);
#16138=ORIENTED_EDGE('',*,*,#12456,.F.);
#16139=ORIENTED_EDGE('',*,*,#12457,.T.);
#16140=ORIENTED_EDGE('',*,*,#12458,.F.);
#16141=ORIENTED_EDGE('',*,*,#12457,.F.);
#16142=ORIENTED_EDGE('',*,*,#12456,.T.);
#16143=ORIENTED_EDGE('',*,*,#12459,.F.);
#16144=ORIENTED_EDGE('',*,*,#12460,.T.);
#16145=ORIENTED_EDGE('',*,*,#12461,.F.);
#16146=ORIENTED_EDGE('',*,*,#12460,.F.);
#16147=ORIENTED_EDGE('',*,*,#12462,.T.);
#16148=ORIENTED_EDGE('',*,*,#12463,.T.);
#16149=ORIENTED_EDGE('',*,*,#12464,.F.);
#16150=ORIENTED_EDGE('',*,*,#12465,.F.);
#16151=ORIENTED_EDGE('',*,*,#12466,.T.);
#16152=ORIENTED_EDGE('',*,*,#12465,.T.);
#16153=ORIENTED_EDGE('',*,*,#12467,.F.);
#16154=ORIENTED_EDGE('',*,*,#12468,.F.);
#16155=ORIENTED_EDGE('',*,*,#12452,.T.);
#16156=ORIENTED_EDGE('',*,*,#12455,.T.);
#16157=ORIENTED_EDGE('',*,*,#12458,.T.);
#16158=ORIENTED_EDGE('',*,*,#12461,.T.);
#16159=ORIENTED_EDGE('',*,*,#12469,.T.);
#16160=ORIENTED_EDGE('',*,*,#12468,.T.);
#16161=ORIENTED_EDGE('',*,*,#12470,.F.);
#16162=ORIENTED_EDGE('',*,*,#12471,.F.);
#16163=ORIENTED_EDGE('',*,*,#12472,.T.);
#16164=ORIENTED_EDGE('',*,*,#12471,.T.);
#16165=ORIENTED_EDGE('',*,*,#12473,.F.);
#16166=ORIENTED_EDGE('',*,*,#12463,.F.);
#16167=ORIENTED_EDGE('',*,*,#12459,.T.);
#16168=ORIENTED_EDGE('',*,*,#12473,.T.);
#16169=ORIENTED_EDGE('',*,*,#12470,.T.);
#16170=ORIENTED_EDGE('',*,*,#12467,.T.);
#16171=ORIENTED_EDGE('',*,*,#12464,.T.);
#16172=ORIENTED_EDGE('',*,*,#12440,.T.);
#16173=ORIENTED_EDGE('',*,*,#12443,.T.);
#16174=ORIENTED_EDGE('',*,*,#12446,.T.);
#16175=ORIENTED_EDGE('',*,*,#12449,.T.);
#16176=ORIENTED_EDGE('',*,*,#12472,.F.);
#16177=ORIENTED_EDGE('',*,*,#12462,.F.);
#16178=ORIENTED_EDGE('',*,*,#12466,.F.);
#16179=ORIENTED_EDGE('',*,*,#12469,.F.);
#21142=CYLINDRICAL_SURFACE('',#24611,0.210000000000001);
#21143=CYLINDRICAL_SURFACE('',#24615,0.210000000000001);
#21144=CYLINDRICAL_SURFACE('',#24619,0.210000000000001);
#21145=CYLINDRICAL_SURFACE('',#24623,0.210000000000001);
#21146=CYLINDRICAL_SURFACE('',#24627,0.165);
#21147=CYLINDRICAL_SURFACE('',#24631,0.165);
#21148=CYLINDRICAL_SURFACE('',#24635,0.165);
#21149=CYLINDRICAL_SURFACE('',#24639,1.11);
#21924=ADVANCED_FACE('',(#3143),#21142,.F.);
#21925=ADVANCED_FACE('',(#3144),#2426,.T.);
#21926=ADVANCED_FACE('',(#3145),#21143,.F.);
#21927=ADVANCED_FACE('',(#3146),#2427,.T.);
#21928=ADVANCED_FACE('',(#3147),#21144,.F.);
#21929=ADVANCED_FACE('',(#3148),#2428,.T.);
#21930=ADVANCED_FACE('',(#3149),#21145,.F.);
#21931=ADVANCED_FACE('',(#3150),#2429,.T.);
#21932=ADVANCED_FACE('',(#3151),#21146,.F.);
#21933=ADVANCED_FACE('',(#3152),#2430,.T.);
#21934=ADVANCED_FACE('',(#3153),#21147,.F.);
#21935=ADVANCED_FACE('',(#3154),#2431,.T.);
#21936=ADVANCED_FACE('',(#3155),#21148,.F.);
#21937=ADVANCED_FACE('',(#3156),#2432,.T.);
#21938=ADVANCED_FACE('',(#3157),#21149,.F.);
#21939=ADVANCED_FACE('',(#3158),#2433,.T.);
#21940=ADVANCED_FACE('',(#3159,#2033,#2034,#2035,#2036),#2434,.T.);
#21941=ADVANCED_FACE('',(#3160),#2435,.T.);
#21942=ADVANCED_FACE('',(#3161,#2037),#2436,.T.);
#21943=ADVANCED_FACE('',(#3162,#2038,#2039,#2040,#2041),#2437,.T.);
#21944=ADVANCED_FACE('',(#3163),#2438,.F.);
#23002=CLOSED_SHELL('',(#21924,#21925,#21926,#21927,#21928,#21929,#21930,
#21931,#21932,#21933,#21934,#21935,#21936,#21937,#21938,#21939,#21940,#21941,
#21942,#21943,#21944));
#24610=AXIS2_PLACEMENT_3D('',#34833,#27954,#27955);
#24611=AXIS2_PLACEMENT_3D('',#34834,#27956,#27957);
#24612=AXIS2_PLACEMENT_3D('',#34836,#27958,#27959);
#24613=AXIS2_PLACEMENT_3D('',#34839,#27961,#27962);
#24614=AXIS2_PLACEMENT_3D('',#34840,#27963,#27964);
#24615=AXIS2_PLACEMENT_3D('',#34841,#27965,#27966);
#24616=AXIS2_PLACEMENT_3D('',#34843,#27967,#27968);
#24617=AXIS2_PLACEMENT_3D('',#34846,#27970,#27971);
#24618=AXIS2_PLACEMENT_3D('',#34847,#27972,#27973);
#24619=AXIS2_PLACEMENT_3D('',#34848,#27974,#27975);
#24620=AXIS2_PLACEMENT_3D('',#34850,#27976,#27977);
#24621=AXIS2_PLACEMENT_3D('',#34853,#27979,#27980);
#24622=AXIS2_PLACEMENT_3D('',#34854,#27981,#27982);
#24623=AXIS2_PLACEMENT_3D('',#34855,#27983,#27984);
#24624=AXIS2_PLACEMENT_3D('',#34857,#27985,#27986);
#24625=AXIS2_PLACEMENT_3D('',#34860,#27988,#27989);
#24626=AXIS2_PLACEMENT_3D('',#34861,#27990,#27991);
#24627=AXIS2_PLACEMENT_3D('',#34862,#27992,#27993);
#24628=AXIS2_PLACEMENT_3D('',#34864,#27994,#27995);
#24629=AXIS2_PLACEMENT_3D('',#34867,#27997,#27998);
#24630=AXIS2_PLACEMENT_3D('',#34868,#27999,#28000);
#24631=AXIS2_PLACEMENT_3D('',#34869,#28001,#28002);
#24632=AXIS2_PLACEMENT_3D('',#34871,#28003,#28004);
#24633=AXIS2_PLACEMENT_3D('',#34874,#28006,#28007);
#24634=AXIS2_PLACEMENT_3D('',#34875,#28008,#28009);
#24635=AXIS2_PLACEMENT_3D('',#34876,#28010,#28011);
#24636=AXIS2_PLACEMENT_3D('',#34878,#28012,#28013);
#24637=AXIS2_PLACEMENT_3D('',#34881,#28015,#28016);
#24638=AXIS2_PLACEMENT_3D('',#34882,#28017,#28018);
#24639=AXIS2_PLACEMENT_3D('',#34883,#28019,#28020);
#24640=AXIS2_PLACEMENT_3D('',#34885,#28021,#28022);
#24641=AXIS2_PLACEMENT_3D('',#34888,#28024,#28025);
#24642=AXIS2_PLACEMENT_3D('',#34889,#28026,#28027);
#24643=AXIS2_PLACEMENT_3D('',#34898,#28032,#28033);
#24644=AXIS2_PLACEMENT_3D('',#34904,#28037,#28038);
#24645=AXIS2_PLACEMENT_3D('',#34910,#28042,#28043);
#24646=AXIS2_PLACEMENT_3D('',#34913,#28046,#28047);
#24647=AXIS2_PLACEMENT_3D('',#34914,#28048,#28049);
#27954=DIRECTION('axis',(0.,0.,1.));
#27955=DIRECTION('refdir',(1.,0.,0.));
#27956=DIRECTION('center_axis',(0.,0.,1.));
#27957=DIRECTION('ref_axis',(1.,0.,0.));
#27958=DIRECTION('center_axis',(0.,0.,1.));
#27959=DIRECTION('ref_axis',(1.,0.,0.));
#27960=DIRECTION('',(0.,0.,1.));
#27961=DIRECTION('center_axis',(0.,0.,-1.));
#27962=DIRECTION('ref_axis',(1.,0.,0.));
#27963=DIRECTION('center_axis',(0.,0.,1.));
#27964=DIRECTION('ref_axis',(1.,0.,0.));
#27965=DIRECTION('center_axis',(0.,0.,1.));
#27966=DIRECTION('ref_axis',(1.,0.,0.));
#27967=DIRECTION('center_axis',(0.,0.,1.));
#27968=DIRECTION('ref_axis',(1.,0.,0.));
#27969=DIRECTION('',(0.,0.,1.));
#27970=DIRECTION('center_axis',(0.,0.,-1.));
#27971=DIRECTION('ref_axis',(1.,0.,0.));
#27972=DIRECTION('center_axis',(0.,0.,1.));
#27973=DIRECTION('ref_axis',(1.,0.,0.));
#27974=DIRECTION('center_axis',(0.,0.,1.));
#27975=DIRECTION('ref_axis',(1.,0.,0.));
#27976=DIRECTION('center_axis',(0.,0.,1.));
#27977=DIRECTION('ref_axis',(1.,0.,0.));
#27978=DIRECTION('',(0.,0.,1.));
#27979=DIRECTION('center_axis',(0.,0.,-1.));
#27980=DIRECTION('ref_axis',(1.,0.,0.));
#27981=DIRECTION('center_axis',(0.,0.,1.));
#27982=DIRECTION('ref_axis',(1.,0.,0.));
#27983=DIRECTION('center_axis',(0.,0.,1.));
#27984=DIRECTION('ref_axis',(1.,0.,0.));
#27985=DIRECTION('center_axis',(0.,0.,1.));
#27986=DIRECTION('ref_axis',(1.,0.,0.));
#27987=DIRECTION('',(0.,0.,1.));
#27988=DIRECTION('center_axis',(0.,0.,-1.));
#27989=DIRECTION('ref_axis',(1.,0.,0.));
#27990=DIRECTION('center_axis',(0.,0.,1.));
#27991=DIRECTION('ref_axis',(1.,0.,0.));
#27992=DIRECTION('center_axis',(1.,0.,0.));
#27993=DIRECTION('ref_axis',(0.,0.,-1.));
#27994=DIRECTION('center_axis',(1.,0.,0.));
#27995=DIRECTION('ref_axis',(0.,0.,-1.));
#27996=DIRECTION('',(1.,0.,0.));
#27997=DIRECTION('center_axis',(-1.,0.,0.));
#27998=DIRECTION('ref_axis',(0.,0.,-1.));
#27999=DIRECTION('center_axis',(1.,0.,0.));
#28000=DIRECTION('ref_axis',(0.,0.,-1.));
#28001=DIRECTION('center_axis',(1.,0.,0.));
#28002=DIRECTION('ref_axis',(0.,0.,-1.));
#28003=DIRECTION('center_axis',(1.,0.,0.));
#28004=DIRECTION('ref_axis',(0.,0.,-1.));
#28005=DIRECTION('',(1.,0.,0.));
#28006=DIRECTION('center_axis',(-1.,0.,0.));
#28007=DIRECTION('ref_axis',(0.,0.,-1.));
#28008=DIRECTION('center_axis',(1.,0.,0.));
#28009=DIRECTION('ref_axis',(0.,0.,-1.));
#28010=DIRECTION('center_axis',(1.,0.,0.));
#28011=DIRECTION('ref_axis',(0.,0.,-1.));
#28012=DIRECTION('center_axis',(1.,0.,0.));
#28013=DIRECTION('ref_axis',(0.,0.,-1.));
#28014=DIRECTION('',(1.,0.,0.));
#28015=DIRECTION('center_axis',(-1.,0.,0.));
#28016=DIRECTION('ref_axis',(0.,0.,-1.));
#28017=DIRECTION('center_axis',(1.,0.,0.));
#28018=DIRECTION('ref_axis',(0.,0.,-1.));
#28019=DIRECTION('center_axis',(1.,0.,0.));
#28020=DIRECTION('ref_axis',(0.,0.,-1.));
#28021=DIRECTION('center_axis',(1.,0.,0.));
#28022=DIRECTION('ref_axis',(0.,0.,-1.));
#28023=DIRECTION('',(1.,0.,0.));
#28024=DIRECTION('center_axis',(-1.,0.,0.));
#28025=DIRECTION('ref_axis',(0.,0.,-1.));
#28026=DIRECTION('center_axis',(0.,1.,0.));
#28027=DIRECTION('ref_axis',(-1.,0.,0.));
#28028=DIRECTION('',(-1.,0.,0.));
#28029=DIRECTION('',(0.,0.,1.));
#28030=DIRECTION('',(-1.,0.,0.));
#28031=DIRECTION('',(0.,0.,1.));
#28032=DIRECTION('center_axis',(1.,0.,0.));
#28033=DIRECTION('ref_axis',(0.,1.,0.));
#28034=DIRECTION('',(0.,1.,0.));
#28035=DIRECTION('',(0.,1.,0.));
#28036=DIRECTION('',(0.,0.,1.));
#28037=DIRECTION('center_axis',(0.,-1.,0.));
#28038=DIRECTION('ref_axis',(1.,0.,0.));
#28039=DIRECTION('',(1.,0.,0.));
#28040=DIRECTION('',(1.,0.,0.));
#28041=DIRECTION('',(0.,0.,1.));
#28042=DIRECTION('center_axis',(-1.,0.,0.));
#28043=DIRECTION('ref_axis',(0.,-1.,0.));
#28044=DIRECTION('',(0.,-1.,0.));
#28045=DIRECTION('',(0.,-1.,0.));
#28046=DIRECTION('center_axis',(0.,0.,1.));
#28047=DIRECTION('ref_axis',(1.,0.,0.));
#28048=DIRECTION('center_axis',(0.,0.,1.));
#28049=DIRECTION('ref_axis',(1.,0.,0.));
#34833=CARTESIAN_POINT('',(0.,0.,0.));
#34834=CARTESIAN_POINT('Origin',(14.,-1.5,5.1));
#34835=CARTESIAN_POINT('',(13.79,-1.5,5.1));
#34836=CARTESIAN_POINT('Origin',(14.,-1.5,5.1));
#34837=CARTESIAN_POINT('',(13.79,-1.5,6.));
#34838=CARTESIAN_POINT('',(13.79,-1.5,5.1));
#34839=CARTESIAN_POINT('Origin',(14.,-1.5,6.));
#34840=CARTESIAN_POINT('Origin',(14.,-1.5,5.1));
#34841=CARTESIAN_POINT('Origin',(12.5,1.5,5.1));
#34842=CARTESIAN_POINT('',(12.29,1.5,5.1));
#34843=CARTESIAN_POINT('Origin',(12.5,1.5,5.1));
#34844=CARTESIAN_POINT('',(12.29,1.5,6.));
#34845=CARTESIAN_POINT('',(12.29,1.5,5.1));
#34846=CARTESIAN_POINT('Origin',(12.5,1.5,6.));
#34847=CARTESIAN_POINT('Origin',(12.5,1.5,5.1));
#34848=CARTESIAN_POINT('Origin',(12.5,-1.5,5.1));
#34849=CARTESIAN_POINT('',(12.29,-1.5,5.1));
#34850=CARTESIAN_POINT('Origin',(12.5,-1.5,5.1));
#34851=CARTESIAN_POINT('',(12.29,-1.5,6.));
#34852=CARTESIAN_POINT('',(12.29,-1.5,5.1));
#34853=CARTESIAN_POINT('Origin',(12.5,-1.5,6.));
#34854=CARTESIAN_POINT('Origin',(12.5,-1.5,5.1));
#34855=CARTESIAN_POINT('Origin',(14.,1.5,5.1));
#34856=CARTESIAN_POINT('',(13.79,1.5,5.1));
#34857=CARTESIAN_POINT('Origin',(14.,1.5,5.1));
#34858=CARTESIAN_POINT('',(13.79,1.5,6.));
#34859=CARTESIAN_POINT('',(13.79,1.5,5.1));
#34860=CARTESIAN_POINT('Origin',(14.,1.5,6.));
#34861=CARTESIAN_POINT('Origin',(14.,1.5,5.1));
#34862=CARTESIAN_POINT('Origin',(12.9,-1.5,4.));
#34863=CARTESIAN_POINT('',(12.9,-1.5,4.165));
#34864=CARTESIAN_POINT('Origin',(12.9,-1.5,4.));
#34865=CARTESIAN_POINT('',(14.5,-1.5,4.165));
#34866=CARTESIAN_POINT('',(12.9,-1.5,4.165));
#34867=CARTESIAN_POINT('Origin',(14.5,-1.5,4.));
#34868=CARTESIAN_POINT('Origin',(12.9,-1.5,4.));
#34869=CARTESIAN_POINT('Origin',(12.9,1.5,4.));
#34870=CARTESIAN_POINT('',(12.9,1.5,4.165));
#34871=CARTESIAN_POINT('Origin',(12.9,1.5,4.));
#34872=CARTESIAN_POINT('',(14.5,1.5,4.165));
#34873=CARTESIAN_POINT('',(12.9,1.5,4.165));
#34874=CARTESIAN_POINT('Origin',(14.5,1.5,4.));
#34875=CARTESIAN_POINT('Origin',(12.9,1.5,4.));
#34876=CARTESIAN_POINT('Origin',(12.9,0.,5.5));
#34877=CARTESIAN_POINT('',(12.9,-2.02066721859313E-17,5.665));
#34878=CARTESIAN_POINT('Origin',(12.9,0.,5.5));
#34879=CARTESIAN_POINT('',(14.5,2.02066721859313E-17,5.665));
#34880=CARTESIAN_POINT('',(12.9,-2.02066721859313E-17,5.665));
#34881=CARTESIAN_POINT('Origin',(14.5,0.,5.5));
#34882=CARTESIAN_POINT('Origin',(12.9,0.,5.5));
#34883=CARTESIAN_POINT('Origin',(11.9,0.,4.));
#34884=CARTESIAN_POINT('',(12.,-1.35935794705356E-16,5.11));
#34885=CARTESIAN_POINT('Origin',(12.,0.,4.));
#34886=CARTESIAN_POINT('',(14.5,1.35935794705356E-16,5.11));
#34887=CARTESIAN_POINT('',(11.9,-1.35935794705356E-16,5.11));
#34888=CARTESIAN_POINT('Origin',(14.5,0.,4.));
#34889=CARTESIAN_POINT('Origin',(14.5,2.2,2.5));
#34890=CARTESIAN_POINT('',(14.5,2.2,2.5));
#34891=CARTESIAN_POINT('',(12.,2.2,2.5));
#34892=CARTESIAN_POINT('',(14.5,2.2,2.5));
#34893=CARTESIAN_POINT('',(12.,2.2,6.));
#34894=CARTESIAN_POINT('',(12.,2.2,2.5));
#34895=CARTESIAN_POINT('',(14.5,2.2,6.));
#34896=CARTESIAN_POINT('',(14.5,2.2,6.));
#34897=CARTESIAN_POINT('',(14.5,2.2,2.5));
#34898=CARTESIAN_POINT('Origin',(14.5,-2.2,2.5));
#34899=CARTESIAN_POINT('',(14.5,-2.2,2.5));
#34900=CARTESIAN_POINT('',(14.5,-2.2,2.5));
#34901=CARTESIAN_POINT('',(14.5,-2.2,6.));
#34902=CARTESIAN_POINT('',(14.5,-2.2,6.));
#34903=CARTESIAN_POINT('',(14.5,-2.2,2.5));
#34904=CARTESIAN_POINT('Origin',(12.,-2.2,2.5));
#34905=CARTESIAN_POINT('',(12.,-2.2,2.5));
#34906=CARTESIAN_POINT('',(12.,-2.2,2.5));
#34907=CARTESIAN_POINT('',(12.,-2.2,6.));
#34908=CARTESIAN_POINT('',(12.,-2.2,6.));
#34909=CARTESIAN_POINT('',(12.,-2.2,2.5));
#34910=CARTESIAN_POINT('Origin',(12.,2.2,2.5));
#34911=CARTESIAN_POINT('',(12.,2.2,2.5));
#34912=CARTESIAN_POINT('',(12.,2.2,6.));
#34913=CARTESIAN_POINT('Origin',(13.25,0.,6.));
#34914=CARTESIAN_POINT('Origin',(13.25,0.,2.5));
#62816=UNCERTAINTY_MEASURE_WITH_UNIT(LENGTH_MEASURE(0.001),#62985,
'DISTANCE_ACCURACY_VALUE',
'Maximum model space distance between geometric entities at asserted c
onnectivities');
#62885=UNCERTAINTY_MEASURE_WITH_UNIT(LENGTH_MEASURE(0.001),#62985,
'DISTANCE_ACCURACY_VALUE',
'Maximum model space distance between geometric entities at asserted c
onnectivities');
#62915=(
GEOMETRIC_REPRESENTATION_CONTEXT(3)
GLOBAL_UNCERTAINTY_ASSIGNED_CONTEXT((#62816))
GLOBAL_UNIT_ASSIGNED_CONTEXT((#62985,#62987,#62988))
REPRESENTATION_CONTEXT('','3D')
);
#62984=(
GEOMETRIC_REPRESENTATION_CONTEXT(3)
GLOBAL_UNCERTAINTY_ASSIGNED_CONTEXT((#62885))
GLOBAL_UNIT_ASSIGNED_CONTEXT((#62985,#62987,#62988))
REPRESENTATION_CONTEXT('','3D')
);
#62985=(
LENGTH_UNIT()
NAMED_UNIT(*)
SI_UNIT(.CENTI.,.METRE.)
);
#62987=(
NAMED_UNIT(*)
PLANE_ANGLE_UNIT()
SI_UNIT($,.RADIAN.)
);
#62988=(
NAMED_UNIT(*)
SI_UNIT($,.STERADIAN.)
SOLID_ANGLE_UNIT()
);
#63018=SHAPE_DEFINITION_REPRESENTATION(#63126,#63378);
#63126=PRODUCT_DEFINITION_SHAPE('',$,#63477);
#63378=SHAPE_REPRESENTATION('',(#24610),#62915);
#63447=PRODUCT_DEFINITION_CONTEXT('part definition',#63743,'design');
#63477=PRODUCT_DEFINITION('X Stage - 07 Nut bracket',
'X Stage - 07 Nut bracket',#63575,#63447);
#63575=PRODUCT_DEFINITION_FORMATION('',$,#63774);
#63743=APPLICATION_CONTEXT(
'Core Data for Automotive Mechanical Design Process');
#63744=PRODUCT_CONTEXT('part definition',#63743,'mechanical');
#63774=PRODUCT('X Stage - 07 Nut bracket','X Stage - 07 Nut bracket',
'X Stage - 07 Nut bracket',(#63744));
#63913=COLOUR_RGB('Black',0.12,0.14,0.17);
#63914=FILL_AREA_STYLE_COLOUR('',#63913);
#63915=FILL_AREA_STYLE('',(#63914));
#63916=SURFACE_STYLE_FILL_AREA(#63915);
#63917=SURFACE_SIDE_STYLE('',(#63916));
#63918=SURFACE_STYLE_USAGE(.BOTH.,#63917);
#63919=PRESENTATION_STYLE_ASSIGNMENT((#63918));
ENDSEC;
END-ISO-10303-21;
